ISO-10303-21;
HEADER;
/* Generated by software containing ST-Developer
 * from STEP Tools, Inc. (www.steptools.com) 
 */

FILE_DESCRIPTION(
/* description */ ('PAT-091'),
/* implementation_level */ '2;1');

FILE_NAME(
/* name */ 'M4 low-profile retaining screw (13).step',
/* time_stamp */ '2026-10-27T15:34:44-07:00',
/* author */ (''),
/* organization */ (''),
/* preprocessor_version */ 'ST-DEVELOPER v20.2',
/* originating_system */ 'Autodesk Translation Framework v15.17.0.0',
/* authorisation */ '');

FILE_SCHEMA (('AUTOMOTIVE_DESIGN { 1 0 10303 214 3 1 1 }'));
ENDSEC;

DATA;
#10=MECHANICAL_DESIGN_GEOMETRIC_PRESENTATION_REPRESENTATION('',(#1067),#25100);
#847=SHAPE_REPRESENTATION_RELATIONSHIP('SRR','None',#25614,#957);
#957=ADVANCED_BREP_SHAPE_REPRESENTATION('',(#1188),#25084);
#1067=STYLED_ITEM('',(#26198),#1188);
#1188=MANIFOLD_SOLID_BREP('Body1',#13347);
#1614=FACE_BOUND('',#3978,.T.);
#2015=PLANE('',#16103);
#2016=PLANE('',#16108);
#2017=PLANE('',#16111);
#2760=FACE_OUTER_BOUND('',#3977,.T.);
#2761=FACE_OUTER_BOUND('',#3979,.T.);
#2762=FACE_OUTER_BOUND('',#3980,.T.);
#2763=FACE_OUTER_BOUND('',#3981,.T.);
#2764=FACE_OUTER_BOUND('',#3982,.T.);
#3977=EDGE_LOOP('',(#11672));
#3978=EDGE_LOOP('',(#11673));
#3979=EDGE_LOOP('',(#11674,#11675,#11676,#11677));
#3980=EDGE_LOOP('',(#11678));
#3981=EDGE_LOOP('',(#11679,#11680,#11681,#11682));
#3982=EDGE_LOOP('',(#11683));
#4828=LINE('',#24156,#5568);
#4829=LINE('',#24160,#5569);
#5568=VECTOR('',#20218,0.350000000000001);
#5569=VECTOR('',#20223,0.199999999999999);
#6246=CIRCLE('',#16104,0.350000000000001);
#6247=CIRCLE('',#16105,0.199999999999999);
#6248=CIRCLE('',#16107,0.350000000000001);
#6249=CIRCLE('',#16110,0.199999999999999);
#7279=VERTEX_POINT('',#24149);
#7280=VERTEX_POINT('',#24151);
#7281=VERTEX_POINT('',#24154);
#7282=VERTEX_POINT('',#24159);
#8771=EDGE_CURVE('',#7279,#7279,#6246,.T.);
#8772=EDGE_CURVE('',#7280,#7280,#6247,.T.);
#8773=EDGE_CURVE('',#7281,#7281,#6248,.T.);
#8774=EDGE_CURVE('',#7281,#7279,#4828,.T.);
#8775=EDGE_CURVE('',#7280,#7282,#4829,.T.);
#8776=EDGE_CURVE('',#7282,#7282,#6249,.T.);
#11672=ORIENTED_EDGE('',*,*,#8771,.F.);
#11673=ORIENTED_EDGE('',*,*,#8772,.T.);
#11674=ORIENTED_EDGE('',*,*,#8773,.F.);
#11675=ORIENTED_EDGE('',*,*,#8774,.T.);
#11676=ORIENTED_EDGE('',*,*,#8771,.T.);
#11677=ORIENTED_EDGE('',*,*,#8774,.F.);
#11678=ORIENTED_EDGE('',*,*,#8773,.T.);
#11679=ORIENTED_EDGE('',*,*,#8772,.F.);
#11680=ORIENTED_EDGE('',*,*,#8775,.T.);
#11681=ORIENTED_EDGE('',*,*,#8776,.T.);
#11682=ORIENTED_EDGE('',*,*,#8775,.F.);
#11683=ORIENTED_EDGE('',*,*,#8776,.F.);
#12384=CYLINDRICAL_SURFACE('',#16106,0.350000000000001);
#12385=CYLINDRICAL_SURFACE('',#16109,0.199999999999999);
#13127=ADVANCED_FACE('',(#2760,#1614),#2015,.F.);
#13128=ADVANCED_FACE('',(#2761),#12384,.T.);
#13129=ADVANCED_FACE('',(#2762),#2016,.T.);
#13130=ADVANCED_FACE('',(#2763),#12385,.T.);
#13131=ADVANCED_FACE('',(#2764),#2017,.F.);
#13347=CLOSED_SHELL('',(#13127,#13128,#13129,#13130,#13131));
#16102=AXIS2_PLACEMENT_3D('',#24147,#20206,#20207);
#16103=AXIS2_PLACEMENT_3D('',#24148,#20208,#20209);
#16104=AXIS2_PLACEMENT_3D('',#24150,#20210,#20211);
#16105=AXIS2_PLACEMENT_3D('',#24152,#20212,#20213);
#16106=AXIS2_PLACEMENT_3D('',#24153,#20214,#20215);
#16107=AXIS2_PLACEMENT_3D('',#24155,#20216,#20217);
#16108=AXIS2_PLACEMENT_3D('',#24157,#20219,#20220);
#16109=AXIS2_PLACEMENT_3D('',#24158,#20221,#20222);
#16110=AXIS2_PLACEMENT_3D('',#24161,#20224,#20225);
#16111=AXIS2_PLACEMENT_3D('',#24162,#20226,#20227);
#20206=DIRECTION('axis',(0.,0.,1.));
#20207=DIRECTION('refdir',(1.,0.,0.));
#20208=DIRECTION('center_axis',(0.,1.,0.));
#20209=DIRECTION('ref_axis',(1.,0.,0.));
#20210=DIRECTION('center_axis',(0.,1.,0.));
#20211=DIRECTION('ref_axis',(1.,0.,0.));
#20212=DIRECTION('center_axis',(0.,1.,0.));
#20213=DIRECTION('ref_axis',(1.,0.,0.));
#20214=DIRECTION('center_axis',(0.,1.,0.));
#20215=DIRECTION('ref_axis',(1.,0.,0.));
#20216=DIRECTION('center_axis',(0.,1.,0.));
#20217=DIRECTION('ref_axis',(1.,0.,0.));
#20218=DIRECTION('',(0.,-1.,0.));
#20219=DIRECTION('center_axis',(0.,1.,0.));
#20220=DIRECTION('ref_axis',(1.,0.,0.));
#20221=DIRECTION('center_axis',(0.,1.,0.));
#20222=DIRECTION('ref_axis',(1.,0.,0.));
#20223=DIRECTION('',(0.,-1.,0.));
#20224=DIRECTION('center_axis',(0.,1.,0.));
#20225=DIRECTION('ref_axis',(1.,0.,0.));
#20226=DIRECTION('center_axis',(0.,1.,0.));
#20227=DIRECTION('ref_axis',(1.,0.,0.));
#24147=CARTESIAN_POINT('',(0.,0.,0.));
#24148=CARTESIAN_POINT('Origin',(18.056769185842,8.3,9.30814754519511));
#24149=CARTESIAN_POINT('',(17.706769185842,8.3,9.30814754519511));
#24150=CARTESIAN_POINT('Origin',(18.056769185842,8.3,9.30814754519511));
#24151=CARTESIAN_POINT('',(17.856769185842,8.3,9.30814754519511));
#24152=CARTESIAN_POINT('Origin',(18.056769185842,8.3,9.30814754519511));
#24153=CARTESIAN_POINT('Origin',(18.056769185842,8.3,9.30814754519511));
#24154=CARTESIAN_POINT('',(17.706769185842,8.4,9.30814754519511));
#24155=CARTESIAN_POINT('Origin',(18.056769185842,8.4,9.30814754519511));
#24156=CARTESIAN_POINT('',(17.706769185842,8.3,9.30814754519511));
#24157=CARTESIAN_POINT('Origin',(18.056769185842,8.4,9.30814754519511));
#24158=CARTESIAN_POINT('Origin',(18.056769185842,7.6,9.30814754519511));
#24159=CARTESIAN_POINT('',(17.856769185842,7.6,9.30814754519511));
#24160=CARTESIAN_POINT('',(17.856769185842,7.6,9.30814754519511));
#24161=CARTESIAN_POINT('Origin',(18.056769185842,7.6,9.30814754519511));
#24162=CARTESIAN_POINT('Origin',(18.056769185842,7.6,9.30814754519511));
#24963=UNCERTAINTY_MEASURE_WITH_UNIT(LENGTH_MEASURE(0.001),#25101,
'DISTANCE_ACCURACY_VALUE',
'Maximum model space distance between geometric entities at asserted c
onnectivities');
#24979=UNCERTAINTY_MEASURE_WITH_UNIT(LENGTH_MEASURE(0.001),#25101,
'DISTANCE_ACCURACY_VALUE',
'Maximum model space distance between geometric entities at asserted c
onnectivities');
#25084=(
GEOMETRIC_REPRESENTATION_CONTEXT(3)
GLOBAL_UNCERTAINTY_ASSIGNED_CONTEXT((#24963))
GLOBAL_UNIT_ASSIGNED_CONTEXT((#25101,#25103,#25104))
REPRESENTATION_CONTEXT('','3D')
);
#25100=(
GEOMETRIC_REPRESENTATION_CONTEXT(3)
GLOBAL_UNCERTAINTY_ASSIGNED_CONTEXT((#24979))
GLOBAL_UNIT_ASSIGNED_CONTEXT((#25101,#25103,#25104))
REPRESENTATION_CONTEXT('','3D')
);
#25101=(
LENGTH_UNIT()
NAMED_UNIT(*)
SI_UNIT(.CENTI.,.METRE.)
);
#25103=(
NAMED_UNIT(*)
PLANE_ANGLE_UNIT()
SI_UNIT($,.RADIAN.)
);
#25104=(
NAMED_UNIT(*)
SI_UNIT($,.STERADIAN.)
SOLID_ANGLE_UNIT()
);
#25209=SHAPE_DEFINITION_REPRESENTATION(#25403,#25614);
#25403=PRODUCT_DEFINITION_SHAPE('',$,#25735);
#25614=SHAPE_REPRESENTATION('',(#16102),#25084);
#25630=PRODUCT_DEFINITION_CONTEXT('part definition',#25992,'design');
#25735=PRODUCT_DEFINITION('M4 low-profile retaining screw (13)',
'M4 low-profile retaining screw (13)',#25855,#25630);
#25855=PRODUCT_DEFINITION_FORMATION('',$,#26098);
#25992=APPLICATION_CONTEXT(
'Core Data for Automotive Mechanical Design Process');
#25993=PRODUCT_CONTEXT('part definition',#25992,'mechanical');
#26098=PRODUCT('M4 low-profile retaining screw (13)',
'M4 low-profile retaining screw (13)','M4 low-profile retaining screw (13)',
(#25993));
#26192=COLOUR_RGB('Black',0.12,0.14,0.17);
#26193=FILL_AREA_STYLE_COLOUR('',#26192);
#26194=FILL_AREA_STYLE('',(#26193));
#26195=SURFACE_STYLE_FILL_AREA(#26194);
#26196=SURFACE_SIDE_STYLE('',(#26195));
#26197=SURFACE_STYLE_USAGE(.BOTH.,#26196);
#26198=PRESENTATION_STYLE_ASSIGNMENT((#26197));
ENDSEC;
END-ISO-10303-21;
